ISO-10303-21;
HEADER;
/* Generated by software containing ST-Developer
 * from STEP Tools, Inc. (www.steptools.com) 
 */

FILE_DESCRIPTION(
/* description */ (''),
/* implementation_level */ '2;1');

FILE_NAME(
/* name */ 'Ring_01.step',
/* time_stamp */ '2026-10-06T13:15:55-07:00',
/* author */ (''),
/* organization */ (''),
/* preprocessor_version */ 'ST-DEVELOPER v20.2',
/* originating_system */ 'Autodesk Translation Framework v15.15.0.0',
/* authorisation */ '');

FILE_SCHEMA (('AUTOMOTIVE_DESIGN { 1 0 10303 214 3 1 1 }'));
ENDSEC;

DATA;
#10=MECHANICAL_DESIGN_GEOMETRIC_PRESENTATION_REPRESENTATION('',(#112),#27707);
#51=TOROIDAL_SURFACE('',#4053,6.1074958342087,0.3);
#52=TOROIDAL_SURFACE('',#4060,6.1071549018742,0.3);
#72=CONICAL_SURFACE('',#4057,6.40732538114918,0.000295609290232334);
#92=SHAPE_REPRESENTATION_RELATIONSHIP('SRR','None',#27749,#102);
#102=ADVANCED_BREP_SHAPE_REPRESENTATION('',(#122),#27701);
#112=STYLED_ITEM('',(#27804),#122);
#122=MANIFOLD_SOLID_BREP('Body1',#3838);
#188=PLANE('',#4059);
#189=PLANE('',#4063);
#242=CIRCLE('',#4054,6.1074958342087);
#243=CIRCLE('',#4055,0.3);
#244=CIRCLE('',#4056,6.40749582110097);
#245=CIRCLE('',#4058,6.40715488876647);
#246=CIRCLE('',#4061,0.3);
#247=CIRCLE('',#4062,6.1071549018742);
#535=FACE_OUTER_BOUND('',#767,.T.);
#536=FACE_OUTER_BOUND('',#768,.T.);
#537=FACE_OUTER_BOUND('',#769,.T.);
#538=FACE_OUTER_BOUND('',#770,.T.);
#539=FACE_OUTER_BOUND('',#771,.T.);
#767=EDGE_LOOP('',(#2973,#2974,#2975,#2976));
#768=EDGE_LOOP('',(#2977,#2978,#2979,#2980));
#769=EDGE_LOOP('',(#2981));
#770=EDGE_LOOP('',(#2982,#2983,#2984,#2985));
#771=EDGE_LOOP('',(#2986));
#1023=LINE('',#7633,#1199);
#1199=VECTOR('',#4602,6.40732538114918);
#1693=VERTEX_POINT('',#7626);
#1694=VERTEX_POINT('',#7628);
#1695=VERTEX_POINT('',#7632);
#1696=VERTEX_POINT('',#7637);
#2156=EDGE_CURVE('',#1693,#1693,#242,.T.);
#2157=EDGE_CURVE('',#1693,#1694,#243,.T.);
#2158=EDGE_CURVE('',#1694,#1694,#244,.T.);
#2159=EDGE_CURVE('',#1694,#1695,#1023,.T.);
#2160=EDGE_CURVE('',#1695,#1695,#245,.T.);
#2161=EDGE_CURVE('',#1695,#1696,#246,.T.);
#2162=EDGE_CURVE('',#1696,#1696,#247,.T.);
#2973=ORIENTED_EDGE('',*,*,#2156,.T.);
#2974=ORIENTED_EDGE('',*,*,#2157,.T.);
#2975=ORIENTED_EDGE('',*,*,#2158,.T.);
#2976=ORIENTED_EDGE('',*,*,#2157,.F.);
#2977=ORIENTED_EDGE('',*,*,#2158,.F.);
#2978=ORIENTED_EDGE('',*,*,#2159,.T.);
#2979=ORIENTED_EDGE('',*,*,#2160,.F.);
#2980=ORIENTED_EDGE('',*,*,#2159,.F.);
#2981=ORIENTED_EDGE('',*,*,#2156,.F.);
#2982=ORIENTED_EDGE('',*,*,#2160,.T.);
#2983=ORIENTED_EDGE('',*,*,#2161,.T.);
#2984=ORIENTED_EDGE('',*,*,#2162,.T.);
#2985=ORIENTED_EDGE('',*,*,#2161,.F.);
#2986=ORIENTED_EDGE('',*,*,#2162,.F.);
#3710=ADVANCED_FACE('',(#535),#51,.T.);
#3711=ADVANCED_FACE('',(#536),#72,.T.);
#3712=ADVANCED_FACE('',(#537),#188,.T.);
#3713=ADVANCED_FACE('',(#538),#52,.T.);
#3714=ADVANCED_FACE('',(#539),#189,.T.);
#3838=CLOSED_SHELL('',(#3710,#3711,#3712,#3713,#3714));
#4052=AXIS2_PLACEMENT_3D('',#7624,#4590,#4591);
#4053=AXIS2_PLACEMENT_3D('',#7625,#4592,#4593);
#4054=AXIS2_PLACEMENT_3D('',#7627,#4594,#4595);
#4055=AXIS2_PLACEMENT_3D('',#7629,#4596,#4597);
#4056=AXIS2_PLACEMENT_3D('',#7630,#4598,#4599);
#4057=AXIS2_PLACEMENT_3D('',#7631,#4600,#4601);
#4058=AXIS2_PLACEMENT_3D('',#7634,#4603,#4604);
#4059=AXIS2_PLACEMENT_3D('',#7635,#4605,#4606);
#4060=AXIS2_PLACEMENT_3D('',#7636,#4607,#4608);
#4061=AXIS2_PLACEMENT_3D('',#7638,#4609,#4610);
#4062=AXIS2_PLACEMENT_3D('',#7639,#4611,#4612);
#4063=AXIS2_PLACEMENT_3D('',#7640,#4613,#4614);
#4590=DIRECTION('axis',(0.,0.,1.));
#4591=DIRECTION('refdir',(1.,0.,0.));
#4592=DIRECTION('center_axis',(1.,0.,0.));
#4593=DIRECTION('ref_axis',(0.,0.,-1.));
#4594=DIRECTION('center_axis',(-1.,0.,0.));
#4595=DIRECTION('ref_axis',(0.,1.22464679914735E-16,1.));
#4596=DIRECTION('center_axis',(0.,-1.,-1.22464679914735E-16));
#4597=DIRECTION('ref_axis',(0.,-1.22464679914735E-16,1.));
#4598=DIRECTION('center_axis',(1.,0.,0.));
#4599=DIRECTION('ref_axis',(0.,0.,1.));
#4600=DIRECTION('center_axis',(1.,0.,0.));
#4601=DIRECTION('ref_axis',(0.,0.,-1.));
#4602=DIRECTION('',(-0.999999956307574,3.62016965808782E-20,-0.000295609285927038));
#4603=DIRECTION('center_axis',(-1.,0.,0.));
#4604=DIRECTION('ref_axis',(0.,0.,1.));
#4605=DIRECTION('center_axis',(1.,0.,0.));
#4606=DIRECTION('ref_axis',(0.,0.,-1.));
#4607=DIRECTION('center_axis',(1.,0.,0.));
#4608=DIRECTION('ref_axis',(0.,0.,-1.));
#4609=DIRECTION('center_axis',(0.,-1.,-1.22464679914735E-16));
#4610=DIRECTION('ref_axis',(0.,-1.22464679914735E-16,1.));
#4611=DIRECTION('center_axis',(1.,0.,0.));
#4612=DIRECTION('ref_axis',(0.,1.22464679914735E-16,1.));
#4613=DIRECTION('center_axis',(-1.,0.,0.));
#4614=DIRECTION('ref_axis',(0.,0.,1.));
#7624=CARTESIAN_POINT('',(0.,0.,0.));
#7625=CARTESIAN_POINT('Origin',(24.2263990006525,0.,0.));
#7626=CARTESIAN_POINT('',(24.5263990006525,-7.47952522416948E-16,6.1074958342087));
#7627=CARTESIAN_POINT('Origin',(24.5263990006525,0.,0.));
#7628=CARTESIAN_POINT('',(24.2263103178667,-7.84691924786135E-16,6.40749582110097));
#7629=CARTESIAN_POINT('Origin',(24.2263990006525,-7.47952522416948E-16,
6.1074958342087));
#7630=CARTESIAN_POINT('Origin',(24.2263103178667,-7.84691924786135E-16,
0.));
#7631=CARTESIAN_POINT('Origin',(23.6497386319918,0.,0.));
#7632=CARTESIAN_POINT('',(23.0729895805454,-7.84650172616918E-16,6.40715488876647));
#7633=CARTESIAN_POINT('',(23.6497386319918,-7.84671051911994E-16,6.40732538114918));
#7634=CARTESIAN_POINT('Origin',(23.0729895805454,-7.84650172616918E-16,
0.));
#7635=CARTESIAN_POINT('Origin',(24.5263990006525,0.,0.));
#7636=CARTESIAN_POINT('Origin',(23.0730782633312,0.,0.));
#7637=CARTESIAN_POINT('',(22.7730782633312,-7.47910770247731E-16,6.1071549018742));
#7638=CARTESIAN_POINT('Origin',(23.0730782633312,-7.47910770247731E-16,
6.1071549018742));
#7639=CARTESIAN_POINT('Origin',(22.7730782633312,0.,0.));
#7640=CARTESIAN_POINT('Origin',(22.7730782633312,0.,-6.40706623219228));
#27689=UNCERTAINTY_MEASURE_WITH_UNIT(LENGTH_MEASURE(0.01),#27708,
'DISTANCE_ACCURACY_VALUE',
'Maximum model space distance between geometric entities at asserted c
onnectivities');
#27695=UNCERTAINTY_MEASURE_WITH_UNIT(LENGTH_MEASURE(0.01),#27708,
'DISTANCE_ACCURACY_VALUE',
'Maximum model space distance between geometric entities at asserted c
onnectivities');
#27701=(
GEOMETRIC_REPRESENTATION_CONTEXT(3)
GLOBAL_UNCERTAINTY_ASSIGNED_CONTEXT((#27689))
GLOBAL_UNIT_ASSIGNED_CONTEXT((#27708,#27710,#27711))
REPRESENTATION_CONTEXT('','3D')
);
#27707=(
GEOMETRIC_REPRESENTATION_CONTEXT(3)
GLOBAL_UNCERTAINTY_ASSIGNED_CONTEXT((#27695))
GLOBAL_UNIT_ASSIGNED_CONTEXT((#27708,#27710,#27711))
REPRESENTATION_CONTEXT('','3D')
);
#27708=(
LENGTH_UNIT()
NAMED_UNIT(*)
SI_UNIT(.MILLI.,.METRE.)
);
#27710=(
NAMED_UNIT(*)
PLANE_ANGLE_UNIT()
SI_UNIT($,.RADIAN.)
);
#27711=(
NAMED_UNIT(*)
SI_UNIT($,.STERADIAN.)
SOLID_ANGLE_UNIT()
);
#27717=SHAPE_DEFINITION_REPRESENTATION(#27728,#27749);
#27728=PRODUCT_DEFINITION_SHAPE('',$,#27761);
#27749=SHAPE_REPRESENTATION('',(#4052),#27701);
#27755=PRODUCT_DEFINITION_CONTEXT('part definition',#27790,'design');
#27761=PRODUCT_DEFINITION('Ring_01','Ring_01',#27772,#27755);
#27772=PRODUCT_DEFINITION_FORMATION('',$,#27797);
#27790=APPLICATION_CONTEXT(
'Core Data for Automotive Mechanical Design Process');
#27791=PRODUCT_CONTEXT('part definition',#27790,'mechanical');
#27797=PRODUCT('Ring_01','Ring_01',$,(#27791));
#27804=PRESENTATION_STYLE_ASSIGNMENT((#27806));
#27806=SURFACE_STYLE_USAGE(.BOTH.,#27808);
#27808=SURFACE_SIDE_STYLE('',(#27810));
#27810=SURFACE_STYLE_FILL_AREA(#27812);
#27812=FILL_AREA_STYLE('Opaque(160,160,160)',(#27814));
#27814=FILL_AREA_STYLE_COLOUR('Opaque(160,160,160)',#27816);
#27816=COLOUR_RGB('Opaque(160,160,160)', 0.09019608, 0.27058824, 0.51372549);
ENDSEC;
END-ISO-10303-21;
